ISO-10303-21;
HEADER;
FILE_DESCRIPTION (('STEP AP203'),
    '1' );
FILE_NAME ('Cleco, Handle, Rivet.step',
    '2026-10-09T13:45:32',
    ( '' ),
    ( '' ),
    'SwSTEP 2.0',
    'SolidWorks 2024',
    '' );
FILE_SCHEMA (( 'AUTOMOTIVE_DESIGN' ));
ENDSEC;

DATA;
#10=FACE_OUTER_BOUND ( 'NONE', #4917, .T. ) ;
#13=FACE_OUTER_BOUND ( 'NONE', #2691, .T. ) ;
#19=VERTEX_POINT ( 'NONE', #3930 ) ;
#39=CIRCLE ( 'NONE', #5286, 0.06200000000000004813 ) ;
#46=DIRECTION ( 'NONE',  ( -0.000000000000000000, -0.000000000000000000, -1.000000000000000000 ) ) ;
#52=CIRCLE ( 'NONE', #6609, 0.1875000000000000278 ) ;
#64=CIRCLE ( 'NONE', #588, 0.1255000000000000282 ) ;
#72=DIRECTION ( 'NONE',  ( 0.000000000000000000, 0.000000000000000000, -1.000000000000000000 ) ) ;
#74=EDGE_CURVE ( 'NONE', #1061, #1984, #3077, .T. ) ;
#78=AXIS2_PLACEMENT_3D ( 'NONE', #1308, #3818, #6319 ) ;
#103=CARTESIAN_POINT ( 'NONE',  ( -0.1250000000000000000, 1.530808498934191509E-17, -0.5599999999999999423 ) ) ;
#114=ORIENTED_EDGE ( 'NONE', *, *, #7639, .F. ) ;
#121=ORIENTED_EDGE ( 'NONE', *, *, #1777, .F. ) ;
#132=DIRECTION ( 'NONE',  ( 0.000000000000000000, 0.000000000000000000, 1.000000000000000000 ) ) ;
#135=DIRECTION ( 'NONE',  ( 1.000000000000000000, 0.000000000000000000, 0.000000000000000000 ) ) ;
#141=VERTEX_POINT ( 'NONE', #7361 ) ;
#149=CARTESIAN_POINT ( 'NONE',  ( 0.1250000000000000000, 0.000000000000000000, -0.5599999999999999423 ) ) ;
#151=EDGE_LOOP ( 'NONE', ( #4432, #6165, #5491, #6432 ) ) ;
#157=FACE_OUTER_BOUND ( 'NONE', #262, .T. ) ;
#159=CIRCLE ( 'NONE', #7494, 0.1255000000000000282 ) ;
#163=TOROIDAL_SURFACE ( 'NONE', #1468, 0.1255000000000000282, 0.06199999999999999956 ) ;
#164=DIRECTION ( 'NONE',  ( -0.000000000000000000, -0.000000000000000000, -1.000000000000000000 ) ) ;
#184=EDGE_LOOP ( 'NONE', ( #3311, #1599, #1452, #4954 ) ) ;
#192=AXIS2_PLACEMENT_3D ( 'NONE', #3731, #7460, #6925 ) ;
#212=CARTESIAN_POINT ( 'NONE',  ( 0.000000000000000000, 0.000000000000000000, 0.000000000000000000 ) ) ;
#223=VECTOR ( 'NONE', #4254, 39.37007874015748143 ) ;
#236=EDGE_CURVE ( 'NONE', #2236, #880, #3736, .T. ) ;
#248=PLANE ( 'NONE',  #4227 ) ;
#250=DIRECTION ( 'NONE',  ( -0.000000000000000000, -0.000000000000000000, 1.000000000000000000 ) ) ;
#255=VERTEX_POINT ( 'NONE', #1363 ) ;
#262=EDGE_LOOP ( 'NONE', ( #7569, #4120, #399, #6373 ) ) ;
#277=EDGE_CURVE ( 'NONE', #2657, #19, #2545, .T. ) ;
#285=EDGE_LOOP ( 'NONE', ( #3269, #3510 ) ) ;
#286=CARTESIAN_POINT ( 'NONE',  ( -0.09374999999999998612, 0.000000000000000000, -0.6537499999999999423 ) ) ;
#312=CARTESIAN_POINT ( 'NONE',  ( 0.000000000000000000, 0.000000000000000000, -0.6219999999999999973 ) ) ;
#326=CLOSED_SHELL ( 'NONE', ( #7293, #1213, #3576, #4699, #7146, #6554, #2083, #770, #1669, #5653, #4136, #4983, #4649, #2467, #682, #1691, #1876, #5950, #2226, #888, #6147, #4446, #7935, #563 ) ) ;
#342=CIRCLE ( 'NONE', #2559, 0.1250000000000000000 ) ;
#343=ORIENTED_EDGE ( 'NONE', *, *, #3532, .F. ) ;
#370=ORIENTED_EDGE ( 'NONE', *, *, #4389, .F. ) ;
#389=DIRECTION ( 'NONE',  ( -1.224646799147353207E-16, 1.000000000000000000, 0.000000000000000000 ) ) ;
#399=ORIENTED_EDGE ( 'NONE', *, *, #277, .F. ) ;
#412=EDGE_CURVE ( 'NONE', #6844, #6487, #6504, .T. ) ;
#429=VECTOR ( 'NONE', #6610, 39.37007874015748143 ) ;
#442=AXIS2_PLACEMENT_3D ( 'NONE', #5974, #2929, #3590 ) ;
#449=CIRCLE ( 'NONE', #1497, 0.06199999999999999956 ) ;
#491=VECTOR ( 'NONE', #6268, 39.37007874015748143 ) ;
#495=CYLINDRICAL_SURFACE ( 'NONE', #3375, 0.1250000000000000000 ) ;
#510=FACE_OUTER_BOUND ( 'NONE', #4661, .T. ) ;
#515=ORIENTED_EDGE ( 'NONE', *, *, #7744, .T. ) ;
#554=TOROIDAL_SURFACE ( 'NONE', #4882, 0.1255000000000000282, 0.06199999999999999956 ) ;
#561=CARTESIAN_POINT ( 'NONE',  ( 0.000000000000000000, 0.000000000000000000, 0.06300000000000000044 ) ) ;
#563=ADVANCED_FACE ( 'NONE', ( #10 ), #723, .T. ) ;
#573=EDGE_CURVE ( 'NONE', #1449, #3669, #5575, .T. ) ;
#588=AXIS2_PLACEMENT_3D ( 'NONE', #2364, #6723, #1107 ) ;
#610=EDGE_LOOP ( 'NONE', ( #3449, #8076, #1071, #6987 ) ) ;
#619=CIRCLE ( 'NONE', #7940, 0.06200000000000004813 ) ;
#646=VERTEX_POINT ( 'NONE', #4410 ) ;
#655=FACE_OUTER_BOUND ( 'NONE', #7525, .T. ) ;
#682=ADVANCED_FACE ( 'NONE', ( #1313 ), #2061, .T. ) ;
#692=ORIENTED_EDGE ( 'NONE', *, *, #5297, .T. ) ;
#702=APPLICATION_CONTEXT ( 'configuration controlled 3d designs of mechanical parts and assemblies' ) ;
#723=TOROIDAL_SURFACE ( 'NONE', #1771, 0.09374999999999998612, 0.03125000000000000000 ) ;
#770=ADVANCED_FACE ( 'NONE', ( #6902 ), #4445, .T. ) ;
#776=CARTESIAN_POINT ( 'NONE',  ( -0.1875000000000000278, 2.296212748401287726E-17, -0.6219999999999999973 ) ) ;
#782=DIRECTION ( 'NONE',  ( -0.000000000000000000, -0.000000000000000000, -1.000000000000000000 ) ) ;
#786=FACE_OUTER_BOUND ( 'NONE', #5326, .T. ) ;
#798=DIRECTION ( 'NONE',  ( 0.000000000000000000, 0.000000000000000000, -1.000000000000000000 ) ) ;
#802=PLANE ( 'NONE',  #7617 ) ;
#830=PRODUCT_DEFINITION ( 'UNKNOWN', '', #4603, #5394 ) ;
#832=EDGE_CURVE ( 'NONE', #3919, #4588, #5185, .T. ) ;
#838=EDGE_CURVE ( 'NONE', #2970, #6487, #342, .T. ) ;
#853=DIRECTION ( 'NONE',  ( 1.000000000000000000, 0.000000000000000000, 0.000000000000000000 ) ) ;
#874=TOROIDAL_SURFACE ( 'NONE', #2041, 0.1255000000000000282, 0.06199999999999999956 ) ;
#875=CIRCLE ( 'NONE', #2054, 0.1875000000000000278 ) ;
#880=VERTEX_POINT ( 'NONE', #1000 ) ;
#888=ADVANCED_FACE ( 'NONE', ( #5380 ), #2826, .T. ) ;
#894=TOROIDAL_SURFACE ( 'NONE', #2581, 0.1255000000000000282, 0.06199999999999999956 ) ;
#909=DIRECTION ( 'NONE',  ( 0.000000000000000000, 0.000000000000000000, 1.000000000000000000 ) ) ;
#919=DIRECTION ( 'NONE',  ( -1.000000000000000000, 0.000000000000000000, 0.000000000000000000 ) ) ;
#941=CARTESIAN_POINT ( 'NONE',  ( 0.000000000000000000, 0.000000000000000000, 0.06199999999999999956 ) ) ;
#944=FACE_OUTER_BOUND ( 'NONE', #1198, .T. ) ;
#949=FACE_BOUND ( 'NONE', #6261, .T. ) ;
#950=DIRECTION ( 'NONE',  ( 1.000000000000000000, 0.000000000000000000, 0.000000000000000000 ) ) ;
#957=CARTESIAN_POINT ( 'NONE',  ( -0.06250000000000000000, 0.000000000000000000, 0.1250000000000000278 ) ) ;
#972=ORIENTED_EDGE ( 'NONE', *, *, #2669, .F. ) ;
#985=EDGE_CURVE ( 'NONE', #6844, #5923, #2953, .T. ) ;
#1000=CARTESIAN_POINT ( 'NONE',  ( -0.1875000000000000278, 0.000000000000000000, 0.06300000000000000044 ) ) ;
#1035=DIRECTION ( 'NONE',  ( 0.000000000000000000, 0.000000000000000000, -1.000000000000000000 ) ) ;
#1054=ORIENTED_EDGE ( 'NONE', *, *, #2781, .T. ) ;
#1061=VERTEX_POINT ( 'NONE', #7902 ) ;
#1070=AXIS2_PLACEMENT_3D ( 'NONE', #3137, #7025, #2668 ) ;
#1071=ORIENTED_EDGE ( 'NONE', *, *, #7393, .T. ) ;
#1073=ORIENTED_EDGE ( 'NONE', *, *, #5287, .F. ) ;
#1094=ORIENTED_EDGE ( 'NONE', *, *, #2742, .T. ) ;
#1097=AXIS2_PLACEMENT_3D ( 'NONE', #7269, #4654, #3504 ) ;
#1107=DIRECTION ( 'NONE',  ( 1.000000000000000000, 0.000000000000000000, 0.000000000000000000 ) ) ;
#1120=( LENGTH_UNIT ( ) NAMED_UNIT ( * ) SI_UNIT ( $, .METRE. ) );
#1145=CARTESIAN_POINT ( 'NONE',  ( 0.09374999999999998612, 0.000000000000000000, 0.1250000000000000000 ) ) ;
#1153=ORIENTED_EDGE ( 'NONE', *, *, #412, .F. ) ;
#1179=EDGE_LOOP ( 'NONE', ( #114, #1692, #343, #5866 ) ) ;
#1198=EDGE_LOOP ( 'NONE', ( #3456, #7345 ) ) ;
#1212=CIRCLE ( 'NONE', #2260, 0.1255000000000000282 ) ;
#1213=ADVANCED_FACE ( 'NONE', ( #157 ), #7540, .T. ) ;
#1231=VERTEX_POINT ( 'NONE', #776 ) ;
#1242=AXIS2_PLACEMENT_3D ( 'NONE', #4527, #7029, #7634 ) ;
#1251=VECTOR ( 'NONE', #1535, 39.37007874015748143 ) ;
#1271=ORIENTED_EDGE ( 'NONE', *, *, #838, .T. ) ;
#1291=EDGE_CURVE ( 'NONE', #6487, #2970, #2561, .T. ) ;
#1308=CARTESIAN_POINT ( 'NONE',  ( 0.000000000000000000, 0.000000000000000000, -0.6537499999999999423 ) ) ;
#1313=FACE_OUTER_BOUND ( 'NONE', #6121, .T. ) ;
#1363=CARTESIAN_POINT ( 'NONE',  ( 0.1255000000000000282, 1.916572240665608148E-17, -0.6849999999999999423 ) ) ;
#1369=APPLICATION_CONTEXT ( 'configuration controlled 3d designs of mechanical parts and assemblies' ) ;
#1376=DIRECTION ( 'NONE',  ( 0.000000000000000000, 0.000000000000000000, 1.000000000000000000 ) ) ;
#1399=CIRCLE ( 'NONE', #5993, 0.06250000000000000000 ) ;
#1416=CARTESIAN_POINT ( 'NONE',  ( 0.06250000000000000000, 7.654042494670957545E-18, 0.09374999999999998612 ) ) ;
#1424=EDGE_CURVE ( 'NONE', #1929, #255, #6112, .T. ) ;
#1438=CARTESIAN_POINT ( 'NONE',  ( 0.000000000000000000, 0.000000000000000000, 0.1250000000000000000 ) ) ;
#1439=PLANE ( 'NONE',  #1601 ) ;
#1445=DIRECTION ( 'NONE',  ( 0.000000000000000000, 0.000000000000000000, -1.000000000000000000 ) ) ;
#1449=VERTEX_POINT ( 'NONE', #1145 ) ;
#1452=ORIENTED_EDGE ( 'NONE', *, *, #2791, .T. ) ;
#1456=DIRECTION ( 'NONE',  ( -0.000000000000000000, -0.000000000000000000, 1.000000000000000000 ) ) ;
#1466=CARTESIAN_POINT ( 'NONE',  ( 0.000000000000000000, 0.000000000000000000, 0.000000000000000000 ) ) ;
#1467=ORIENTED_EDGE ( 'NONE', *, *, #7639, .T. ) ;
#1468=AXIS2_PLACEMENT_3D ( 'NONE', #6681, #6164, #2415 ) ;
#1478=DIRECTION ( 'NONE',  ( 0.000000000000000000, 0.000000000000000000, 1.000000000000000000 ) ) ;
#1482=AXIS2_PLACEMENT_3D ( 'NONE', #7574, #3810, #72 ) ;
#1493=ORIENTED_EDGE ( 'NONE', *, *, #2362, .T. ) ;
#1494=ORIENTED_EDGE ( 'NONE', *, *, #2362, .F. ) ;
#1497=AXIS2_PLACEMENT_3D ( 'NONE', #1580, #389, #5891 ) ;
#1506=CARTESIAN_POINT ( 'NONE',  ( 0.000000000000000000, 0.000000000000000000, -0.6849999999999999423 ) ) ;
#1535=DIRECTION ( 'NONE',  ( 0.000000000000000000, 0.000000000000000000, 1.000000000000000000 ) ) ;
#1558=DIRECTION ( 'NONE',  ( 1.000000000000000000, 0.000000000000000000, 0.000000000000000000 ) ) ;
#1565=DIRECTION ( 'NONE',  ( 0.000000000000000000, 0.000000000000000000, 1.000000000000000000 ) ) ;
#1580=CARTESIAN_POINT ( 'NONE',  ( 0.1255000000000000282, 1.536931732929928570E-17, -0.6219999999999999973 ) ) ;
#1583=FACE_OUTER_BOUND ( 'NONE', #7438, .T. ) ;
#1599=ORIENTED_EDGE ( 'NONE', *, *, #4190, .F. ) ;
#1601=AXIS2_PLACEMENT_3D ( 'NONE', #212, #132, #3058 ) ;
#1613=AXIS2_PLACEMENT_3D ( 'NONE', #286, #2788, #2248 ) ;
#1620=DIRECTION ( 'NONE',  ( -1.000000000000000000, 0.000000000000000000, 0.000000000000000000 ) ) ;
#1628=FACE_BOUND ( 'NONE', #4643, .T. ) ;
#1643=CARTESIAN_POINT ( 'NONE',  ( 0.000000000000000000, 0.000000000000000000, 0.06300000000000000044 ) ) ;
#1655=AXIS2_PLACEMENT_3D ( 'NONE', #7962, #5432, #6219 ) ;
#1669=ADVANCED_FACE ( 'NONE', ( #7649 ), #4018, .T. ) ;
#1686=DIRECTION ( 'NONE',  ( 0.000000000000000000, -1.000000000000000000, 0.000000000000000000 ) ) ;
#1691=ADVANCED_FACE ( 'NONE', ( #5936, #3357 ), #802, .T. ) ;
#1692=ORIENTED_EDGE ( 'NONE', *, *, #1424, .T. ) ;
#1699=DIRECTION ( 'NONE',  ( 0.000000000000000000, 0.000000000000000000, 1.000000000000000000 ) ) ;
#1745=CARTESIAN_POINT ( 'NONE',  ( 0.06250000000000000000, 7.654042494670957545E-18, 0.1250000000000000278 ) ) ;
#1758=DIRECTION ( 'NONE',  ( 1.000000000000000000, 0.000000000000000000, 0.000000000000000000 ) ) ;
#1771=AXIS2_PLACEMENT_3D ( 'NONE', #5011, #4858, #4285 ) ;
#1777=EDGE_CURVE ( 'NONE', #1231, #6526, #2639, .T. ) ;
#1778=AXIS2_PLACEMENT_3D ( 'NONE', #1438, #4474, #3284 ) ;
#1779=ORIENTED_EDGE ( 'NONE', *, *, #6697, .F. ) ;
#1804=DIRECTION ( 'NONE',  ( -0.000000000000000000, -0.000000000000000000, 1.000000000000000000 ) ) ;
#1807=CARTESIAN_POINT ( 'NONE',  ( 0.1255000000000000282, 1.916572240665608148E-17, -0.5599999999999999423 ) ) ;
#1810=FACE_OUTER_BOUND ( 'NONE', #1179, .T. ) ;
#1814=EDGE_LOOP ( 'NONE', ( #1467, #6817, #4111, #2431 ) ) ;
#1820=ORIENTED_EDGE ( 'NONE', *, *, #7744, .F. ) ;
#1845=CARTESIAN_POINT ( 'NONE',  ( 0.000000000000000000, 0.000000000000000000, -0.6229999999999998872 ) ) ;
#1855=ORIENTED_EDGE ( 'NONE', *, *, #7975, .F. ) ;
#1859=DIRECTION ( 'NONE',  ( -1.000000000000000000, 0.000000000000000000, 0.000000000000000000 ) ) ;
#1876=ADVANCED_FACE ( 'NONE', ( #786, #5562 ), #1439, .F. ) ;
#1880=EDGE_CURVE ( 'NONE', #4588, #3919, #159, .T. ) ;
#1881=VECTOR ( 'NONE', #3647, 39.37007874015748143 ) ;
#1919=CIRCLE ( 'NONE', #7925, 0.1250000000000000000 ) ;
#1929=VERTEX_POINT ( 'NONE', #5224 ) ;
#1941=EDGE_CURVE ( 'NONE', #880, #3919, #2514, .T. ) ;
#1942=SHAPE_REPRESENTATION ( 'Cleco, Handle, Rivet', ( #3555 ), #6058 ) ;
#1984=VERTEX_POINT ( 'NONE', #4812 ) ;
#2003=CARTESIAN_POINT ( 'NONE',  ( 0.000000000000000000, 0.000000000000000000, 0.09374999999999998612 ) ) ;
#2007=DIRECTION ( 'NONE',  ( -1.000000000000000000, 0.000000000000000000, 0.000000000000000000 ) ) ;
#2025=AXIS2_PLACEMENT_3D ( 'NONE', #7889, #5985, #2244 ) ;
#2028=EDGE_CURVE ( 'NONE', #5362, #2657, #7145, .T. ) ;
#2041=AXIS2_PLACEMENT_3D ( 'NONE', #7611, #4434, #5772 ) ;
#2046=AXIS2_PLACEMENT_3D ( 'NONE', #1466, #5214, #1558 ) ;
#2054=AXIS2_PLACEMENT_3D ( 'NONE', #5119, #250, #7585 ) ;
#2061=CYLINDRICAL_SURFACE ( 'NONE', #1778, 0.1875000000000000278 ) ;
#2063=AXIS2_PLACEMENT_3D ( 'NONE', #3898, #3241, #3200 ) ;
#2065=DIRECTION ( 'NONE',  ( -0.000000000000000000, -0.000000000000000000, -1.000000000000000000 ) ) ;
#2083=ADVANCED_FACE ( 'NONE', ( #2874 ), #554, .T. ) ;
#2090=DIRECTION ( 'NONE',  ( 1.000000000000000000, 0.000000000000000000, 0.000000000000000000 ) ) ;
#2105=CARTESIAN_POINT ( 'NONE',  ( 0.1255000000000000282, 0.000000000000000000, 0.06300000000000000044 ) ) ;
#2106=DIRECTION ( 'NONE',  ( -1.000000000000000000, 0.000000000000000000, 0.000000000000000000 ) ) ;
#2126=CARTESIAN_POINT ( 'NONE',  ( 0.000000000000000000, 0.000000000000000000, -0.6849999999999999423 ) ) ;
#2129=ORIENTED_EDGE ( 'NONE', *, *, #236, .F. ) ;
#2158=ORIENTED_EDGE ( 'NONE', *, *, #7741, .F. ) ;
#2173=FACE_OUTER_BOUND ( 'NONE', #7893, .T. ) ;
#2177=ORIENTED_EDGE ( 'NONE', *, *, #2028, .T. ) ;
#2206=CARTESIAN_POINT ( 'NONE',  ( 0.1875000000000000278, 0.000000000000000000, -0.6219999999999999973 ) ) ;
#2224=ORIENTED_EDGE ( 'NONE', *, *, #1291, .F. ) ;
#2226=ADVANCED_FACE ( 'NONE', ( #8023 ), #163, .T. ) ;
#2236=VERTEX_POINT ( 'NONE', #4929 ) ;
#2244=DIRECTION ( 'NONE',  ( -1.000000000000000000, 0.000000000000000000, -0.000000000000000000 ) ) ;
#2248=DIRECTION ( 'NONE',  ( 0.000000000000000000, 0.000000000000000000, -1.000000000000000000 ) ) ;
#2260=AXIS2_PLACEMENT_3D ( 'NONE', #3411, #4064, #3371 ) ;
#2301=AXIS2_PLACEMENT_3D ( 'NONE', #4518, #3330, #7060 ) ;
#2310=AXIS2_PLACEMENT_3D ( 'NONE', #2859, #7812, #7170 ) ;
#2356=DIRECTION ( 'NONE',  ( -1.000000000000000000, 0.000000000000000000, 0.000000000000000000 ) ) ;
#2362=EDGE_CURVE ( 'NONE', #6459, #5362, #6060, .T. ) ;
#2364=CARTESIAN_POINT ( 'NONE',  ( 0.000000000000000000, 0.000000000000000000, 0.000000000000000000 ) ) ;
#2375=EDGE_LOOP ( 'NONE', ( #4312, #2427, #5262, #5637 ) ) ;
#2384=AXIS2_PLACEMENT_3D ( 'NONE', #2003, #4470, #7711 ) ;
#2415=DIRECTION ( 'NONE',  ( 1.000000000000000000, 0.000000000000000000, 0.000000000000000000 ) ) ;
#2427=ORIENTED_EDGE ( 'NONE', *, *, #412, .T. ) ;
#2430=ORIENTED_EDGE ( 'NONE', *, *, #1880, .F. ) ;
#2431=ORIENTED_EDGE ( 'NONE', *, *, #2723, .F. ) ;
#2432=EDGE_CURVE ( 'NONE', #5830, #4799, #1212, .T. ) ;
#2441=AXIS2_PLACEMENT_3D ( 'NONE', #3905, #6401, #3938 ) ;
#2467=ADVANCED_FACE ( 'NONE', ( #6601, #949 ), #248, .F. ) ;
#2509=CYLINDRICAL_SURFACE ( 'NONE', #8032, 0.1250000000000000000 ) ;
#2514=CIRCLE ( 'NONE', #3310, 0.06199999999999999956 ) ;
#2524=EDGE_CURVE ( 'NONE', #1061, #2657, #6973, .T. ) ;
#2545=CIRCLE ( 'NONE', #3602, 0.06250000000000000000 ) ;
#2555=DIRECTION ( 'NONE',  ( -1.000000000000000000, 0.000000000000000000, 0.000000000000000000 ) ) ;
#2559=AXIS2_PLACEMENT_3D ( 'NONE', #7826, #1478, #4153 ) ;
#2561=CIRCLE ( 'NONE', #2046, 0.1250000000000000000 ) ;
#2581=AXIS2_PLACEMENT_3D ( 'NONE', #1845, #3000, #5499 ) ;
#2607=DIRECTION ( 'NONE',  ( 0.000000000000000000, 0.000000000000000000, 1.000000000000000000 ) ) ;
#2639=CIRCLE ( 'NONE', #5790, 0.1875000000000000278 ) ;
#2651=DIRECTION ( 'NONE',  ( -0.000000000000000000, -0.000000000000000000, 1.000000000000000000 ) ) ;
#2657=VERTEX_POINT ( 'NONE', #4839 ) ;
#2661=CARTESIAN_POINT ( 'NONE',  ( 0.000000000000000000, 0.000000000000000000, 0.1250000000000000000 ) ) ;
#2668=DIRECTION ( 'NONE',  ( -1.000000000000000000, 0.000000000000000000, 0.000000000000000000 ) ) ;
#2669=EDGE_CURVE ( 'NONE', #880, #2236, #7506, .T. ) ;
#2691=EDGE_LOOP ( 'NONE', ( #1153, #8022, #1054, #2224 ) ) ;
#2712=CIRCLE ( 'NONE', #2063, 0.03125000000000000694 ) ;
#2714=ORIENTED_EDGE ( 'NONE', *, *, #2986, .T. ) ;
#2719=CARTESIAN_POINT ( 'NONE',  ( 0.000000000000000000, 0.000000000000000000, 0.09374999999999998612 ) ) ;
#2723=EDGE_CURVE ( 'NONE', #1929, #6526, #4918, .T. ) ;
#2733=CARTESIAN_POINT ( 'NONE',  ( 0.000000000000000000, 0.000000000000000000, 0.1250000000000000000 ) ) ;
#2740=CARTESIAN_POINT ( 'NONE',  ( 0.000000000000000000, 0.000000000000000000, -0.6219999999999999973 ) ) ;
#2742=EDGE_CURVE ( 'NONE', #4799, #1231, #39, .T. ) ;
#2757=DIRECTION ( 'NONE',  ( 1.000000000000000000, 0.000000000000000000, 0.000000000000000000 ) ) ;
#2781=EDGE_CURVE ( 'NONE', #5923, #2970, #4547, .T. ) ;
#2788=DIRECTION ( 'NONE',  ( -0.000000000000000000, -1.000000000000000000, -0.000000000000000000 ) ) ;
#2791=EDGE_CURVE ( 'NONE', #3779, #2877, #3181, .T. ) ;
#2793=DIRECTION ( 'NONE',  ( -0.000000000000000000, -0.000000000000000000, 1.000000000000000000 ) ) ;
#2820=DIRECTION ( 'NONE',  ( 0.000000000000000000, 0.000000000000000000, -1.000000000000000000 ) ) ;
#2826=TOROIDAL_SURFACE ( 'NONE', #6495, 0.1255000000000000282, 0.06199999999999999956 ) ;
#2828=CARTESIAN_POINT ( 'NONE',  ( 0.000000000000000000, 0.000000000000000000, -0.5599999999999999423 ) ) ;
#2844=CIRCLE ( 'NONE', #3373, 0.03125000000000000000 ) ;
#2852=CIRCLE ( 'NONE', #7031, 0.06199999999999999956 ) ;
#2859=CARTESIAN_POINT ( 'NONE',  ( 0.000000000000000000, 0.000000000000000000, 0.06199999999999999956 ) ) ;
#2874=FACE_OUTER_BOUND ( 'NONE', #6890, .T. ) ;
#2877=VERTEX_POINT ( 'NONE', #5109 ) ;
#2929=DIRECTION ( 'NONE',  ( -0.000000000000000000, -0.000000000000000000, 1.000000000000000000 ) ) ;
#2953=CIRCLE ( 'NONE', #7795, 0.1250000000000000000 ) ;
#2970=VERTEX_POINT ( 'NONE', #5979 ) ;
#2971=AXIS2_PLACEMENT_3D ( 'NONE', #6174, #8039, #1859 ) ;
#2986=EDGE_CURVE ( 'NONE', #141, #2877, #6850, .T. ) ;
#3000=DIRECTION ( 'NONE',  ( 0.000000000000000000, 0.000000000000000000, -1.000000000000000000 ) ) ;
#3007=LENGTH_MEASURE_WITH_UNIT ( LENGTH_MEASURE( 0.02539999999999999897 ), #1120 );
#3058=DIRECTION ( 'NONE',  ( -1.000000000000000000, 0.000000000000000000, 0.000000000000000000 ) ) ;
#3067=DIRECTION ( 'NONE',  ( -0.000000000000000000, -0.000000000000000000, -1.000000000000000000 ) ) ;
#3070=AXIS2_PLACEMENT_3D ( 'NONE', #7666, #164, #950 ) ;
#3077=CIRCLE ( 'NONE', #5960, 0.09374999999999998612 ) ;
#3107=AXIS2_PLACEMENT_3D ( 'NONE', #6356, #2607, #3274 ) ;
#3117=TOROIDAL_SURFACE ( 'NONE', #7034, 0.09374999999999998612, 0.03125000000000000000 ) ;
#3119=ORIENTED_EDGE ( 'NONE', *, *, #1880, .T. ) ;
#3137=CARTESIAN_POINT ( 'NONE',  ( 0.000000000000000000, 0.000000000000000000, -0.6537499999999999423 ) ) ;
#3149=ORIENTED_EDGE ( 'NONE', *, *, #3936, .F. ) ;
#3157=SHAPE_DEFINITION_REPRESENTATION ( #3552, #1942 ) ;
#3170=ORIENTED_EDGE ( 'NONE', *, *, #3936, .T. ) ;
#3181=CIRCLE ( 'NONE', #1482, 0.06199999999999999956 ) ;
#3184=CARTESIAN_POINT ( 'NONE',  ( -0.1875000000000000278, 2.296212748401287726E-17, -0.6849999999999999423 ) ) ;
#3200=DIRECTION ( 'NONE',  ( -1.000000000000000000, 1.224646799147352961E-16, 0.000000000000000000 ) ) ;
#3206=DIRECTION ( 'NONE',  ( -1.000000000000000000, 0.000000000000000000, 0.000000000000000000 ) ) ;
#3241=DIRECTION ( 'NONE',  ( 1.224646799147353207E-16, 1.000000000000000000, -0.000000000000000000 ) ) ;
#3249=FACE_OUTER_BOUND ( 'NONE', #151, .T. ) ;
#3268=CARTESIAN_POINT ( 'NONE',  ( -0.1255000000000000282, 0.000000000000000000, -0.6219999999999999973 ) ) ;
#3269=ORIENTED_EDGE ( 'NONE', *, *, #5287, .T. ) ;
#3274=DIRECTION ( 'NONE',  ( 1.000000000000000000, 0.000000000000000000, 0.000000000000000000 ) ) ;
#3279=EDGE_CURVE ( 'NONE', #7259, #141, #4628, .T. ) ;
#3284=DIRECTION ( 'NONE',  ( -1.000000000000000000, 0.000000000000000000, 0.000000000000000000 ) ) ;
#3287=DIRECTION ( 'NONE',  ( 1.000000000000000000, 0.000000000000000000, 0.000000000000000000 ) ) ;
#3310=AXIS2_PLACEMENT_3D ( 'NONE', #8046, #3333, #5832 ) ;
#3311=ORIENTED_EDGE ( 'NONE', *, *, #3279, .F. ) ;
#3315=ORIENTED_EDGE ( 'NONE', *, *, #2432, .F. ) ;
#3316=VECTOR ( 'NONE', #1804, 39.37007874015748143 ) ;
#3326=CARTESIAN_POINT ( 'NONE',  ( 0.000000000000000000, 0.000000000000000000, -0.5599999999999999423 ) ) ;
#3330=DIRECTION ( 'NONE',  ( -0.000000000000000000, -0.000000000000000000, -1.000000000000000000 ) ) ;
#3331=AXIS2_PLACEMENT_3D ( 'NONE', #6501, #7632, #2555 ) ;
#3333=DIRECTION ( 'NONE',  ( 1.224646799147353207E-16, 1.000000000000000000, -0.000000000000000000 ) ) ;
#3357=FACE_OUTER_BOUND ( 'NONE', #5537, .T. ) ;
#3371=DIRECTION ( 'NONE',  ( -1.000000000000000000, 0.000000000000000000, 0.000000000000000000 ) ) ;
#3373=AXIS2_PLACEMENT_3D ( 'NONE', #7404, #4864, #4781 ) ;
#3375=AXIS2_PLACEMENT_3D ( 'NONE', #7376, #6195, #4843 ) ;
#3389=DIRECTION ( 'NONE',  ( 0.000000000000000000, 0.000000000000000000, -1.000000000000000000 ) ) ;
#3411=CARTESIAN_POINT ( 'NONE',  ( 0.000000000000000000, 0.000000000000000000, -0.5599999999999999423 ) ) ;
#3440=DIRECTION ( 'NONE',  ( -1.000000000000000000, 0.000000000000000000, 0.000000000000000000 ) ) ;
#3449=ORIENTED_EDGE ( 'NONE', *, *, #2669, .T. ) ;
#3456=ORIENTED_EDGE ( 'NONE', *, *, #3532, .T. ) ;
#3504=DIRECTION ( 'NONE',  ( -1.000000000000000000, 1.224646799147352714E-16, 0.000000000000000000 ) ) ;
#3510=ORIENTED_EDGE ( 'NONE', *, *, #2432, .T. ) ;
#3531=DIRECTION ( 'NONE',  ( 0.000000000000000000, 0.000000000000000000, 1.000000000000000000 ) ) ;
#3532=EDGE_CURVE ( 'NONE', #646, #255, #6603, .T. ) ;
#3552=PRODUCT_DEFINITION_SHAPE ( 'NONE', 'NONE',  #830 ) ;
#3555=AXIS2_PLACEMENT_3D ( 'NONE', #5720, #6981, #135 ) ;
#3575=MANIFOLD_SOLID_BREP ( 'Fillet2', #326 ) ;
#3576=ADVANCED_FACE ( 'NONE', ( #3249 ), #6900, .F. ) ;
#3586=AXIS2_PLACEMENT_3D ( 'NONE', #6341, #798, #7724 ) ;
#3590=DIRECTION ( 'NONE',  ( 1.000000000000000000, 0.000000000000000000, 0.000000000000000000 ) ) ;
#3598=AXIS2_PLACEMENT_3D ( 'NONE', #5670, #4473, #2007 ) ;
#3602=AXIS2_PLACEMENT_3D ( 'NONE', #4487, #1445, #2106 ) ;
#3647=DIRECTION ( 'NONE',  ( -0.000000000000000000, -0.000000000000000000, 1.000000000000000000 ) ) ;
#3669=VERTEX_POINT ( 'NONE', #6935 ) ;
#3672=ORIENTED_EDGE ( 'NONE', *, *, #2524, .T. ) ;
#3696=ORIENTED_EDGE ( 'NONE', *, *, #74, .T. ) ;
#3731=CARTESIAN_POINT ( 'NONE',  ( 0.000000000000000000, 0.000000000000000000, 0.1250000000000000278 ) ) ;
#3736=CIRCLE ( 'NONE', #1242, 0.1875000000000000278 ) ;
#3764=CIRCLE ( 'NONE', #2971, 0.1255000000000000282 ) ;
#3779=VERTEX_POINT ( 'NONE', #4573 ) ;
#3791=EDGE_CURVE ( 'NONE', #6526, #1231, #4247, .T. ) ;
#3810=DIRECTION ( 'NONE',  ( 0.000000000000000000, -1.000000000000000000, 0.000000000000000000 ) ) ;
#3818=DIRECTION ( 'NONE',  ( 0.000000000000000000, 0.000000000000000000, -1.000000000000000000 ) ) ;
#3864=CARTESIAN_POINT ( 'NONE',  ( 0.000000000000000000, 0.000000000000000000, 0.1250000000000000278 ) ) ;
#3867=CARTESIAN_POINT ( 'NONE',  ( 0.000000000000000000, 0.000000000000000000, 0.1250000000000000000 ) ) ;
#3898=CARTESIAN_POINT ( 'NONE',  ( -0.09374999999999998612, 1.148106374200643401E-17, 0.09374999999999998612 ) ) ;
#3905=CARTESIAN_POINT ( 'NONE',  ( 0.09374999999999998612, 0.000000000000000000, 0.09374999999999998612 ) ) ;
#3908=DIRECTION ( 'NONE',  ( 0.000000000000000000, 0.000000000000000000, 1.000000000000000000 ) ) ;
#3910=LINE ( 'NONE', #4522, #6960 ) ;
#3911=CARTESIAN_POINT ( 'NONE',  ( -0.06250000000000000000, 0.000000000000000000, 0.09374999999999998612 ) ) ;
#3919=VERTEX_POINT ( 'NONE', #4825 ) ;
#3922=DIRECTION ( 'NONE',  ( -1.000000000000000000, 0.000000000000000000, 0.000000000000000000 ) ) ;
#3930=CARTESIAN_POINT ( 'NONE',  ( 0.06250000000000000000, 7.654042494670957545E-18, -0.6537499999999999423 ) ) ;
#3936=EDGE_CURVE ( 'NONE', #5830, #6526, #449, .T. ) ;
#3938=DIRECTION ( 'NONE',  ( 0.000000000000000000, 0.000000000000000000, -1.000000000000000000 ) ) ;
#3962=CARTESIAN_POINT ( 'NONE',  ( -0.1250000000000000000, 1.530808498934191509E-17, 0.000000000000000000 ) ) ;
#4018=CYLINDRICAL_SURFACE ( 'NONE', #4222, 0.1875000000000000278 ) ;
#4064=DIRECTION ( 'NONE',  ( -0.000000000000000000, -0.000000000000000000, 1.000000000000000000 ) ) ;
#4111=ORIENTED_EDGE ( 'NONE', *, *, #1777, .T. ) ;
#4120=ORIENTED_EDGE ( 'NONE', *, *, #6697, .T. ) ;
#4136=ADVANCED_FACE ( 'NONE', ( #13 ), #2509, .T. ) ;
#4150=DIRECTION ( 'NONE',  ( -0.000000000000000000, -1.000000000000000000, -0.000000000000000000 ) ) ;
#4151=TOROIDAL_SURFACE ( 'NONE', #2310, 0.1255000000000000282, 0.06199999999999999956 ) ;
#4152=AXIS2_PLACEMENT_3D ( 'NONE', #2661, #782, #6437 ) ;
#4153=DIRECTION ( 'NONE',  ( 1.000000000000000000, 0.000000000000000000, 0.000000000000000000 ) ) ;
#4177=CARTESIAN_POINT ( 'NONE',  ( 0.1255000000000000282, 1.536931732929928570E-17, -0.6229999999999998872 ) ) ;
#4182=EDGE_CURVE ( 'NONE', #4299, #1929, #52, .T. ) ;
#4186=MECHANICAL_CONTEXT ( 'NONE', #1369, 'mechanical' ) ;
#4187=ORIENTED_EDGE ( 'NONE', *, *, #2723, .T. ) ;
#4190=EDGE_CURVE ( 'NONE', #3779, #7259, #6738, .T. ) ;
#4193=EDGE_LOOP ( 'NONE', ( #1271, #7804 ) ) ;
#4210=ORIENTED_EDGE ( 'NONE', *, *, #8072, .F. ) ;
#4222=AXIS2_PLACEMENT_3D ( 'NONE', #1506, #1456, #853 ) ;
#4227=AXIS2_PLACEMENT_3D ( 'NONE', #2828, #5338, #4712 ) ;
#4247=CIRCLE ( 'NONE', #3586, 0.1875000000000000278 ) ;
#4254=DIRECTION ( 'NONE',  ( -0.000000000000000000, -0.000000000000000000, -1.000000000000000000 ) ) ;
#4261=TOROIDAL_SURFACE ( 'NONE', #5312, 0.1255000000000000282, 0.06199999999999999956 ) ;
#4263=CARTESIAN_POINT ( 'NONE',  ( -0.1255000000000000282, 0.000000000000000000, -0.5599999999999999423 ) ) ;
#4279=ORIENTED_EDGE ( 'NONE', *, *, #7261, .T. ) ;
#4280=AXIS2_PLACEMENT_3D ( 'NONE', #2740, #4671, #3440 ) ;
#4285=DIRECTION ( 'NONE',  ( 1.000000000000000000, 0.000000000000000000, 0.000000000000000000 ) ) ;
#4295=EDGE_LOOP ( 'NONE', ( #5034, #6013, #6456, #1855 ) ) ;
#4299=VERTEX_POINT ( 'NONE', #4593 ) ;
#4312=ORIENTED_EDGE ( 'NONE', *, *, #7635, .T. ) ;
#4331=ORIENTED_EDGE ( 'NONE', *, *, #4833, .F. ) ;
#4389=EDGE_CURVE ( 'NONE', #7259, #3779, #64, .T. ) ;
#4405=ORIENTED_EDGE ( 'NONE', *, *, #236, .T. ) ;
#4410=CARTESIAN_POINT ( 'NONE',  ( -0.1255000000000000282, 0.000000000000000000, -0.6849999999999999423 ) ) ;
#4423=TOROIDAL_SURFACE ( 'NONE', #1655, 0.09374999999999998612, 0.03125000000000000000 ) ;
#4427=LINE ( 'NONE', #3184, #1881 ) ;
#4432=ORIENTED_EDGE ( 'NONE', *, *, #7047, .T. ) ;
#4434=DIRECTION ( 'NONE',  ( 0.000000000000000000, 0.000000000000000000, 1.000000000000000000 ) ) ;
#4445=CYLINDRICAL_SURFACE ( 'NONE', #2301, 0.1875000000000000278 ) ;
#4446=ADVANCED_FACE ( 'NONE', ( #655 ), #8016, .F. ) ;
#4468=CARTESIAN_POINT ( 'NONE',  ( -0.1255000000000000282, 1.916572240665608148E-17, 0.000000000000000000 ) ) ;
#4470=DIRECTION ( 'NONE',  ( 0.000000000000000000, 0.000000000000000000, 1.000000000000000000 ) ) ;
#4473=DIRECTION ( 'NONE',  ( 0.000000000000000000, 0.000000000000000000, -1.000000000000000000 ) ) ;
#4474=DIRECTION ( 'NONE',  ( -0.000000000000000000, -0.000000000000000000, -1.000000000000000000 ) ) ;
#4487=CARTESIAN_POINT ( 'NONE',  ( 0.000000000000000000, 0.000000000000000000, -0.6537499999999999423 ) ) ;
#4508=FACE_OUTER_BOUND ( 'NONE', #4631, .T. ) ;
#4518=CARTESIAN_POINT ( 'NONE',  ( 0.000000000000000000, 0.000000000000000000, 0.1250000000000000000 ) ) ;
#4522=CARTESIAN_POINT ( 'NONE',  ( 0.1875000000000000278, 2.296212748401287726E-17, 0.1250000000000000000 ) ) ;
#4527=CARTESIAN_POINT ( 'NONE',  ( 0.000000000000000000, 0.000000000000000000, 0.06300000000000000044 ) ) ;
#4543=CIRCLE ( 'NONE', #3107, 0.1875000000000000278 ) ;
#4547=LINE ( 'NONE', #149, #4888 ) ;
#4560=DIRECTION ( 'NONE',  ( -0.000000000000000000, -0.000000000000000000, 1.000000000000000000 ) ) ;
#4573=CARTESIAN_POINT ( 'NONE',  ( 0.1255000000000000282, 0.000000000000000000, 0.000000000000000000 ) ) ;
#4588=VERTEX_POINT ( 'NONE', #7609 ) ;
#4593=CARTESIAN_POINT ( 'NONE',  ( -0.1875000000000000278, 2.296212748401287726E-17, -0.6229999999999998872 ) ) ;
#4603=PRODUCT_DEFINITION_FORMATION_WITH_SPECIFIED_SOURCE ( 'ANY', '', #7731, .NOT_KNOWN. ) ;
#4613=ORIENTED_EDGE ( 'NONE', *, *, #1941, .T. ) ;
#4628=CIRCLE ( 'NONE', #1097, 0.06199999999999999956 ) ;
#4631=EDGE_LOOP ( 'NONE', ( #1820, #4279, #1494, #2158 ) ) ;
#4637=AXIS2_PLACEMENT_3D ( 'NONE', #3864, #46, #7059 ) ;
#4643=EDGE_LOOP ( 'NONE', ( #3696, #692 ) ) ;
#4649=ADVANCED_FACE ( 'NONE', ( #1628, #944 ), #4834, .T. ) ;
#4654=DIRECTION ( 'NONE',  ( 1.224646799147353207E-16, 1.000000000000000000, -0.000000000000000000 ) ) ;
#4661=EDGE_LOOP ( 'NONE', ( #1779, #6477, #3672, #6732 ) ) ;
#4671=DIRECTION ( 'NONE',  ( 0.000000000000000000, 0.000000000000000000, -1.000000000000000000 ) ) ;
#4691=ORIENTED_EDGE ( 'NONE', *, *, #985, .F. ) ;
#4699=ADVANCED_FACE ( 'NONE', ( #6022 ), #4261, .T. ) ;
#4712=DIRECTION ( 'NONE',  ( -1.000000000000000000, 0.000000000000000000, -0.000000000000000000 ) ) ;
#4720=ORIENTED_EDGE ( 'NONE', *, *, #832, .T. ) ;
#4745=DIRECTION ( 'NONE',  ( 1.000000000000000000, 0.000000000000000000, 0.000000000000000000 ) ) ;
#4762=CARTESIAN_POINT ( 'NONE',  ( -0.1255000000000000282, 0.000000000000000000, -0.6229999999999998872 ) ) ;
#4781=DIRECTION ( 'NONE',  ( -1.000000000000000000, -1.224646799147353207E-16, 0.000000000000000000 ) ) ;
#4796=DIRECTION ( 'NONE',  ( -1.224646799147353207E-16, 1.000000000000000000, 0.000000000000000000 ) ) ;
#4799=VERTEX_POINT ( 'NONE', #4263 ) ;
#4812=CARTESIAN_POINT ( 'NONE',  ( 0.09374999999999998612, 1.148106374200643401E-17, -0.6849999999999999423 ) ) ;
#4816=( NAMED_UNIT ( * ) PLANE_ANGLE_UNIT ( ) SI_UNIT ( $, .RADIAN. ) );
#4825=CARTESIAN_POINT ( 'NONE',  ( -0.1255000000000000282, 1.916572240665608148E-17, 0.1250000000000000000 ) ) ;
#4833=EDGE_CURVE ( 'NONE', #4299, #1231, #4427, .T. ) ;
#4834=PLANE ( 'NONE',  #2025 ) ;
#4839=CARTESIAN_POINT ( 'NONE',  ( -0.06250000000000000000, 0.000000000000000000, -0.6537499999999999423 ) ) ;
#4843=DIRECTION ( 'NONE',  ( 1.000000000000000000, 0.000000000000000000, 0.000000000000000000 ) ) ;
#4845=ORIENTED_EDGE ( 'NONE', *, *, #7393, .F. ) ;
#4858=DIRECTION ( 'NONE',  ( 0.000000000000000000, 0.000000000000000000, 1.000000000000000000 ) ) ;
#4864=DIRECTION ( 'NONE',  ( -1.224646799147353207E-16, 1.000000000000000000, 0.000000000000000000 ) ) ;
#4882=AXIS2_PLACEMENT_3D ( 'NONE', #1643, #3531, #5418 ) ;
#4888=VECTOR ( 'NONE', #1376, 39.37007874015748143 ) ;
#4917=EDGE_LOOP ( 'NONE', ( #6334, #6834, #6439, #6607 ) ) ;
#4918=LINE ( 'NONE', #7417, #3316 ) ;
#4929=CARTESIAN_POINT ( 'NONE',  ( 0.1875000000000000278, 2.296212748401287726E-17, 0.06300000000000000044 ) ) ;
#4930=AXIS2_PLACEMENT_3D ( 'NONE', #4177, #4796, #4957 ) ;
#4954=ORIENTED_EDGE ( 'NONE', *, *, #2986, .F. ) ;
#4957=DIRECTION ( 'NONE',  ( -1.000000000000000000, -1.224646799147353207E-16, 0.000000000000000000 ) ) ;
#4983=ADVANCED_FACE ( 'NONE', ( #7201 ), #6625, .T. ) ;
#4994=DIMENSIONAL_EXPONENTS ( 1.000000000000000000, 0.000000000000000000, 0.000000000000000000, 0.000000000000000000, 0.000000000000000000, 0.000000000000000000, 0.000000000000000000 ) ;
#5011=CARTESIAN_POINT ( 'NONE',  ( 0.000000000000000000, 0.000000000000000000, 0.09374999999999998612 ) ) ;
#5014=CARTESIAN_POINT ( 'NONE',  ( 0.000000000000000000, 0.000000000000000000, -0.5599999999999999423 ) ) ;
#5034=ORIENTED_EDGE ( 'NONE', *, *, #1424, .F. ) ;
#5063=CARTESIAN_POINT ( 'NONE',  ( 0.000000000000000000, 0.000000000000000000, -0.6849999999999999423 ) ) ;
#5109=CARTESIAN_POINT ( 'NONE',  ( 0.1875000000000000278, 2.296212748401287726E-17, 0.06199999999999999956 ) ) ;
#5119=CARTESIAN_POINT ( 'NONE',  ( 0.000000000000000000, 0.000000000000000000, -0.6229999999999998872 ) ) ;
#5185=CIRCLE ( 'NONE', #5710, 0.1255000000000000282 ) ;
#5214=DIRECTION ( 'NONE',  ( 0.000000000000000000, 0.000000000000000000, 1.000000000000000000 ) ) ;
#5223=DIRECTION ( 'NONE',  ( 0.000000000000000000, 0.000000000000000000, -1.000000000000000000 ) ) ;
#5224=CARTESIAN_POINT ( 'NONE',  ( 0.1875000000000000278, 0.000000000000000000, -0.6229999999999998872 ) ) ;
#5234=EDGE_LOOP ( 'NONE', ( #7159, #2129, #6073, #6197 ) ) ;
#5254=DIRECTION ( 'NONE',  ( 0.000000000000000000, 0.000000000000000000, 1.000000000000000000 ) ) ;
#5262=ORIENTED_EDGE ( 'NONE', *, *, #838, .F. ) ;
#5268=CIRCLE ( 'NONE', #1070, 0.06250000000000000000 ) ;
#5286=AXIS2_PLACEMENT_3D ( 'NONE', #3268, #6923, #7608 ) ;
#5287=EDGE_CURVE ( 'NONE', #4799, #5830, #7903, .T. ) ;
#5297=EDGE_CURVE ( 'NONE', #1984, #1061, #7895, .T. ) ;
#5312=AXIS2_PLACEMENT_3D ( 'NONE', #5484, #7970, #2356 ) ;
#5326=EDGE_LOOP ( 'NONE', ( #7725, #6277 ) ) ;
#5338=DIRECTION ( 'NONE',  ( 0.000000000000000000, 0.000000000000000000, -1.000000000000000000 ) ) ;
#5346=CARTESIAN_POINT ( 'NONE',  ( 0.000000000000000000, 0.000000000000000000, 0.1250000000000000000 ) ) ;
#5362=VERTEX_POINT ( 'NONE', #3911 ) ;
#5380=FACE_OUTER_BOUND ( 'NONE', #4295, .T. ) ;
#5394=DESIGN_CONTEXT ( 'detailed design', #702, 'design' ) ;
#5418=DIRECTION ( 'NONE',  ( 1.000000000000000000, 0.000000000000000000, 0.000000000000000000 ) ) ;
#5432=DIRECTION ( 'NONE',  ( 0.000000000000000000, 0.000000000000000000, -1.000000000000000000 ) ) ;
#5484=CARTESIAN_POINT ( 'NONE',  ( 0.000000000000000000, 0.000000000000000000, -0.6219999999999999973 ) ) ;
#5491=ORIENTED_EDGE ( 'NONE', *, *, #8081, .T. ) ;
#5499=DIRECTION ( 'NONE',  ( -1.000000000000000000, 0.000000000000000000, 0.000000000000000000 ) ) ;
#5510=ORIENTED_EDGE ( 'NONE', *, *, #3279, .T. ) ;
#5537=EDGE_LOOP ( 'NONE', ( #3119, #4720 ) ) ;
#5562=FACE_BOUND ( 'NONE', #4193, .T. ) ;
#5575=CIRCLE ( 'NONE', #5708, 0.09374999999999998612 ) ;
#5637=ORIENTED_EDGE ( 'NONE', *, *, #2781, .F. ) ;
#5642=CARTESIAN_POINT ( 'NONE',  ( -0.1875000000000000278, 0.000000000000000000, 0.1250000000000000000 ) ) ;
#5653=ADVANCED_FACE ( 'NONE', ( #7977 ), #495, .T. ) ;
#5670=CARTESIAN_POINT ( 'NONE',  ( 0.000000000000000000, 0.000000000000000000, -0.6849999999999999423 ) ) ;
#5677=CARTESIAN_POINT ( 'NONE',  ( 0.000000000000000000, 0.000000000000000000, -0.6229999999999998872 ) ) ;
#5708=AXIS2_PLACEMENT_3D ( 'NONE', #7350, #7993, #6695 ) ;
#5710=AXIS2_PLACEMENT_3D ( 'NONE', #5346, #1565, #7262 ) ;
#5718=CIRCLE ( 'NONE', #2441, 0.03125000000000000000 ) ;
#5720=CARTESIAN_POINT ( 'NONE',  ( 0.000000000000000000, 0.000000000000000000, 0.000000000000000000 ) ) ;
#5770=ORIENTED_EDGE ( 'NONE', *, *, #2791, .F. ) ;
#5772=DIRECTION ( 'NONE',  ( 1.000000000000000000, 0.000000000000000000, 0.000000000000000000 ) ) ;
#5790=AXIS2_PLACEMENT_3D ( 'NONE', #312, #2820, #7813 ) ;
#5812=DIRECTION ( 'NONE',  ( 0.000000000000000000, 0.000000000000000000, 1.000000000000000000 ) ) ;
#5830=VERTEX_POINT ( 'NONE', #1807 ) ;
#5832=DIRECTION ( 'NONE',  ( -1.000000000000000000, 1.224646799147352714E-16, 0.000000000000000000 ) ) ;
#5866=ORIENTED_EDGE ( 'NONE', *, *, #7091, .F. ) ;
#5891=DIRECTION ( 'NONE',  ( -1.000000000000000000, -1.224646799147353207E-16, 0.000000000000000000 ) ) ;
#5911=ORIENTED_EDGE ( 'NONE', *, *, #277, .T. ) ;
#5923=VERTEX_POINT ( 'NONE', #6315 ) ;
#5936=FACE_BOUND ( 'NONE', #7240, .T. ) ;
#5950=ADVANCED_FACE ( 'NONE', ( #7081 ), #874, .T. ) ;
#5960=AXIS2_PLACEMENT_3D ( 'NONE', #2126, #2651, #1620 ) ;
#5974=CARTESIAN_POINT ( 'NONE',  ( 0.000000000000000000, 0.000000000000000000, -0.6849999999999999423 ) ) ;
#5979=CARTESIAN_POINT ( 'NONE',  ( 0.1250000000000000000, 0.000000000000000000, 0.000000000000000000 ) ) ;
#5985=DIRECTION ( 'NONE',  ( 0.000000000000000000, 0.000000000000000000, -1.000000000000000000 ) ) ;
#5993=AXIS2_PLACEMENT_3D ( 'NONE', #2719, #7682, #2757 ) ;
#6013=ORIENTED_EDGE ( 'NONE', *, *, #4182, .F. ) ;
#6014=ORIENTED_EDGE ( 'NONE', *, *, #6936, .F. ) ;
#6022=FACE_OUTER_BOUND ( 'NONE', #6648, .T. ) ;
#6032=CARTESIAN_POINT ( 'NONE',  ( 0.000000000000000000, 0.000000000000000000, -0.6229999999999998872 ) ) ;
#6035=EDGE_LOOP ( 'NONE', ( #4331, #6799, #4187, #7134 ) ) ;
#6053=LINE ( 'NONE', #1745, #223 ) ;
#6058=( GEOMETRIC_REPRESENTATION_CONTEXT ( 3 ) GLOBAL_UNCERTAINTY_ASSIGNED_CONTEXT ( ( #6862 ) ) GLOBAL_UNIT_ASSIGNED_CONTEXT ( ( #7989, #4816, #6689 ) ) REPRESENTATION_CONTEXT ( 'NONE', 'WORKASPACE' ) );
#6060=CIRCLE ( 'NONE', #2384, 0.06250000000000000000 ) ;
#6073=ORIENTED_EDGE ( 'NONE', *, *, #6936, .T. ) ;
#6075=DIRECTION ( 'NONE',  ( -0.000000000000000000, -0.000000000000000000, 1.000000000000000000 ) ) ;
#6112=CIRCLE ( 'NONE', #4930, 0.06199999999999999956 ) ;
#6121=EDGE_LOOP ( 'NONE', ( #4210, #4405, #6851, #2714 ) ) ;
#6147=ADVANCED_FACE ( 'NONE', ( #2173 ), #7160, .T. ) ;
#6164=DIRECTION ( 'NONE',  ( 0.000000000000000000, 0.000000000000000000, 1.000000000000000000 ) ) ;
#6165=ORIENTED_EDGE ( 'NONE', *, *, #6756, .T. ) ;
#6173=DIRECTION ( 'NONE',  ( 1.000000000000000000, 0.000000000000000000, 0.000000000000000000 ) ) ;
#6174=CARTESIAN_POINT ( 'NONE',  ( 0.000000000000000000, 0.000000000000000000, -0.6849999999999999423 ) ) ;
#6195=DIRECTION ( 'NONE',  ( 0.000000000000000000, 0.000000000000000000, 1.000000000000000000 ) ) ;
#6197=ORIENTED_EDGE ( 'NONE', *, *, #832, .F. ) ;
#6219=DIRECTION ( 'NONE',  ( -1.000000000000000000, 0.000000000000000000, 0.000000000000000000 ) ) ;
#6261=EDGE_LOOP ( 'NONE', ( #6576, #4691 ) ) ;
#6268=DIRECTION ( 'NONE',  ( -0.000000000000000000, -0.000000000000000000, -1.000000000000000000 ) ) ;
#6277=ORIENTED_EDGE ( 'NONE', *, *, #4389, .T. ) ;
#6315=CARTESIAN_POINT ( 'NONE',  ( 0.1250000000000000000, 0.000000000000000000, -0.5599999999999999423 ) ) ;
#6319=DIRECTION ( 'NONE',  ( -1.000000000000000000, 0.000000000000000000, 0.000000000000000000 ) ) ;
#6325=AXIS2_PLACEMENT_3D ( 'NONE', #561, #3067, #1758 ) ;
#6334=ORIENTED_EDGE ( 'NONE', *, *, #7261, .F. ) ;
#6341=CARTESIAN_POINT ( 'NONE',  ( 0.000000000000000000, 0.000000000000000000, -0.6219999999999999973 ) ) ;
#6356=CARTESIAN_POINT ( 'NONE',  ( 0.000000000000000000, 0.000000000000000000, 0.06199999999999999956 ) ) ;
#6373=ORIENTED_EDGE ( 'NONE', *, *, #2524, .F. ) ;
#6401=DIRECTION ( 'NONE',  ( 0.000000000000000000, -1.000000000000000000, 0.000000000000000000 ) ) ;
#6432=ORIENTED_EDGE ( 'NONE', *, *, #2028, .F. ) ;
#6437=DIRECTION ( 'NONE',  ( 1.000000000000000000, 0.000000000000000000, 0.000000000000000000 ) ) ;
#6439=ORIENTED_EDGE ( 'NONE', *, *, #7741, .T. ) ;
#6456=ORIENTED_EDGE ( 'NONE', *, *, #7091, .T. ) ;
#6459=VERTEX_POINT ( 'NONE', #1416 ) ;
#6472=AXIS2_PLACEMENT_3D ( 'NONE', #5063, #6947, #7680 ) ;
#6477=ORIENTED_EDGE ( 'NONE', *, *, #74, .F. ) ;
#6487=VERTEX_POINT ( 'NONE', #3962 ) ;
#6495=AXIS2_PLACEMENT_3D ( 'NONE', #6032, #5223, #7793 ) ;
#6501=CARTESIAN_POINT ( 'NONE',  ( 0.000000000000000000, 0.000000000000000000, -0.5599999999999999423 ) ) ;
#6504=LINE ( 'NONE', #7226, #1251 ) ;
#6526=VERTEX_POINT ( 'NONE', #2206 ) ;
#6554=ADVANCED_FACE ( 'NONE', ( #1583 ), #4151, .T. ) ;
#6576=ORIENTED_EDGE ( 'NONE', *, *, #7635, .F. ) ;
#6601=FACE_OUTER_BOUND ( 'NONE', #285, .T. ) ;
#6603=CIRCLE ( 'NONE', #3598, 0.1255000000000000282 ) ;
#6607=ORIENTED_EDGE ( 'NONE', *, *, #7047, .F. ) ;
#6609=AXIS2_PLACEMENT_3D ( 'NONE', #5677, #2793, #919 ) ;
#6610=DIRECTION ( 'NONE',  ( -0.000000000000000000, -0.000000000000000000, -1.000000000000000000 ) ) ;
#6625=CYLINDRICAL_SURFACE ( 'NONE', #442, 0.1875000000000000278 ) ;
#6648=EDGE_LOOP ( 'NONE', ( #3315, #3170, #121, #7806 ) ) ;
#6655=ORIENTED_EDGE ( 'NONE', *, *, #6756, .F. ) ;
#6681=CARTESIAN_POINT ( 'NONE',  ( 0.000000000000000000, 0.000000000000000000, 0.06199999999999999956 ) ) ;
#6689=( NAMED_UNIT ( * ) SI_UNIT ( $, .STERADIAN. ) SOLID_ANGLE_UNIT ( ) );
#6695=DIRECTION ( 'NONE',  ( 1.000000000000000000, 0.000000000000000000, 0.000000000000000000 ) ) ;
#6697=EDGE_CURVE ( 'NONE', #1984, #19, #2844, .T. ) ;
#6723=DIRECTION ( 'NONE',  ( -0.000000000000000000, -0.000000000000000000, -1.000000000000000000 ) ) ;
#6728=DIRECTION ( 'NONE',  ( -1.000000000000000000, 0.000000000000000000, 0.000000000000000000 ) ) ;
#6732=ORIENTED_EDGE ( 'NONE', *, *, #8081, .F. ) ;
#6738=CIRCLE ( 'NONE', #3070, 0.1255000000000000282 ) ;
#6756=EDGE_CURVE ( 'NONE', #6459, #19, #6053, .T. ) ;
#6794=EDGE_CURVE ( 'NONE', #880, #141, #7520, .T. ) ;
#6799=ORIENTED_EDGE ( 'NONE', *, *, #4182, .T. ) ;
#6817=ORIENTED_EDGE ( 'NONE', *, *, #4833, .T. ) ;
#6834=ORIENTED_EDGE ( 'NONE', *, *, #573, .F. ) ;
#6844=VERTEX_POINT ( 'NONE', #103 ) ;
#6850=CIRCLE ( 'NONE', #7886, 0.1875000000000000278 ) ;
#6851=ORIENTED_EDGE ( 'NONE', *, *, #6794, .T. ) ;
#6862=UNCERTAINTY_MEASURE_WITH_UNIT (LENGTH_MEASURE( 1.000000000000000082E-05 ), #7989, 'distance_accuracy_value', 'NONE');
#6890=EDGE_LOOP ( 'NONE', ( #972, #4613, #2430, #6014 ) ) ;
#6897=ORIENTED_EDGE ( 'NONE', *, *, #573, .T. ) ;
#6900=CYLINDRICAL_SURFACE ( 'NONE', #4637, 0.06250000000000000000 ) ;
#6902=FACE_OUTER_BOUND ( 'NONE', #610, .T. ) ;
#6923=DIRECTION ( 'NONE',  ( -0.000000000000000000, -1.000000000000000000, -0.000000000000000000 ) ) ;
#6925=DIRECTION ( 'NONE',  ( -1.000000000000000000, 0.000000000000000000, 0.000000000000000000 ) ) ;
#6935=CARTESIAN_POINT ( 'NONE',  ( -0.09374999999999998612, 1.148106374200643401E-17, 0.1250000000000000000 ) ) ;
#6936=EDGE_CURVE ( 'NONE', #2236, #4588, #2852, .T. ) ;
#6947=DIRECTION ( 'NONE',  ( -0.000000000000000000, -0.000000000000000000, 1.000000000000000000 ) ) ;
#6960=VECTOR ( 'NONE', #2065, 39.37007874015748143 ) ;
#6966=CARTESIAN_POINT ( 'NONE',  ( 0.000000000000000000, 0.000000000000000000, 0.09374999999999998612 ) ) ;
#6973=CIRCLE ( 'NONE', #1613, 0.03124999999999997571 ) ;
#6981=DIRECTION ( 'NONE',  ( 0.000000000000000000, 0.000000000000000000, 1.000000000000000000 ) ) ;
#6987=ORIENTED_EDGE ( 'NONE', *, *, #6794, .F. ) ;
#7023=CIRCLE ( 'NONE', #4152, 0.09374999999999998612 ) ;
#7025=DIRECTION ( 'NONE',  ( 0.000000000000000000, 0.000000000000000000, -1.000000000000000000 ) ) ;
#7029=DIRECTION ( 'NONE',  ( -0.000000000000000000, -0.000000000000000000, -1.000000000000000000 ) ) ;
#7031=AXIS2_PLACEMENT_3D ( 'NONE', #2105, #1686, #3389 ) ;
#7034=AXIS2_PLACEMENT_3D ( 'NONE', #6966, #5254, #2090 ) ;
#7047=EDGE_CURVE ( 'NONE', #5362, #6459, #1399, .T. ) ;
#7059=DIRECTION ( 'NONE',  ( -1.000000000000000000, 0.000000000000000000, 0.000000000000000000 ) ) ;
#7060=DIRECTION ( 'NONE',  ( -1.000000000000000000, 0.000000000000000000, 0.000000000000000000 ) ) ;
#7081=FACE_OUTER_BOUND ( 'NONE', #5234, .T. ) ;
#7091=EDGE_CURVE ( 'NONE', #4299, #646, #619, .T. ) ;
#7134=ORIENTED_EDGE ( 'NONE', *, *, #3791, .T. ) ;
#7145=LINE ( 'NONE', #957, #429 ) ;
#7146=ADVANCED_FACE ( 'NONE', ( #1810 ), #894, .T. ) ;
#7159=ORIENTED_EDGE ( 'NONE', *, *, #1941, .F. ) ;
#7160=TOROIDAL_SURFACE ( 'NONE', #4280, 0.1255000000000000282, 0.06199999999999999956 ) ;
#7170=DIRECTION ( 'NONE',  ( 1.000000000000000000, 0.000000000000000000, 0.000000000000000000 ) ) ;
#7180=ADVANCED_BREP_SHAPE_REPRESENTATION ( '', ( #3575, #3555 ), #6058 ) ;
#7201=FACE_OUTER_BOUND ( 'NONE', #6035, .T. ) ;
#7226=CARTESIAN_POINT ( 'NONE',  ( -0.1250000000000000000, 1.530808498934191509E-17, -0.5599999999999999423 ) ) ;
#7240=EDGE_LOOP ( 'NONE', ( #6897, #515 ) ) ;
#7259=VERTEX_POINT ( 'NONE', #4468 ) ;
#7261=EDGE_CURVE ( 'NONE', #3669, #5362, #2712, .T. ) ;
#7262=DIRECTION ( 'NONE',  ( 1.000000000000000000, 0.000000000000000000, 0.000000000000000000 ) ) ;
#7269=CARTESIAN_POINT ( 'NONE',  ( -0.1255000000000000282, 1.536931732929928570E-17, 0.06199999999999999956 ) ) ;
#7293=ADVANCED_FACE ( 'NONE', ( #4508 ), #3117, .T. ) ;
#7312=SHAPE_REPRESENTATION_RELATIONSHIP ( 'NONE' , 'NONE' ,  #1942, #7180 ) ;
#7338=CARTESIAN_POINT ( 'NONE',  ( 0.000000000000000000, 0.000000000000000000, -0.5599999999999999423 ) ) ;
#7345=ORIENTED_EDGE ( 'NONE', *, *, #7975, .T. ) ;
#7350=CARTESIAN_POINT ( 'NONE',  ( 0.000000000000000000, 0.000000000000000000, 0.1250000000000000000 ) ) ;
#7361=CARTESIAN_POINT ( 'NONE',  ( -0.1875000000000000278, 0.000000000000000000, 0.06199999999999999956 ) ) ;
#7376=CARTESIAN_POINT ( 'NONE',  ( 0.000000000000000000, 0.000000000000000000, -0.5599999999999999423 ) ) ;
#7393=EDGE_CURVE ( 'NONE', #2877, #141, #4543, .T. ) ;
#7404=CARTESIAN_POINT ( 'NONE',  ( 0.09374999999999998612, 1.148106374200643401E-17, -0.6537499999999999423 ) ) ;
#7417=CARTESIAN_POINT ( 'NONE',  ( 0.1875000000000000278, 0.000000000000000000, -0.6849999999999999423 ) ) ;
#7438=EDGE_LOOP ( 'NONE', ( #370, #5510, #4845, #5770 ) ) ;
#7460=DIRECTION ( 'NONE',  ( -0.000000000000000000, -0.000000000000000000, -1.000000000000000000 ) ) ;
#7494=AXIS2_PLACEMENT_3D ( 'NONE', #3867, #3908, #3287 ) ;
#7506=CIRCLE ( 'NONE', #6325, 0.1875000000000000278 ) ;
#7520=LINE ( 'NONE', #5642, #491 ) ;
#7525=EDGE_LOOP ( 'NONE', ( #6655, #1493, #2177, #5911 ) ) ;
#7533=ORIENTED_EDGE ( 'NONE', *, *, #3791, .F. ) ;
#7540=TOROIDAL_SURFACE ( 'NONE', #78, 0.09374999999999998612, 0.03125000000000000000 ) ;
#7569=ORIENTED_EDGE ( 'NONE', *, *, #5297, .F. ) ;
#7574=CARTESIAN_POINT ( 'NONE',  ( 0.1255000000000000282, 0.000000000000000000, 0.06199999999999999956 ) ) ;
#7585=DIRECTION ( 'NONE',  ( -1.000000000000000000, 0.000000000000000000, 0.000000000000000000 ) ) ;
#7608=DIRECTION ( 'NONE',  ( 0.000000000000000000, 0.000000000000000000, -1.000000000000000000 ) ) ;
#7609=CARTESIAN_POINT ( 'NONE',  ( 0.1255000000000000282, 0.000000000000000000, 0.1250000000000000000 ) ) ;
#7611=CARTESIAN_POINT ( 'NONE',  ( 0.000000000000000000, 0.000000000000000000, 0.06300000000000000044 ) ) ;
#7617=AXIS2_PLACEMENT_3D ( 'NONE', #2733, #909, #3922 ) ;
#7632=DIRECTION ( 'NONE',  ( -0.000000000000000000, -0.000000000000000000, 1.000000000000000000 ) ) ;
#7634=DIRECTION ( 'NONE',  ( 1.000000000000000000, 0.000000000000000000, 0.000000000000000000 ) ) ;
#7635=EDGE_CURVE ( 'NONE', #5923, #6844, #1919, .T. ) ;
#7639=EDGE_CURVE ( 'NONE', #1929, #4299, #875, .T. ) ;
#7649=FACE_OUTER_BOUND ( 'NONE', #1814, .T. ) ;
#7666=CARTESIAN_POINT ( 'NONE',  ( 0.000000000000000000, 0.000000000000000000, 0.000000000000000000 ) ) ;
#7680=DIRECTION ( 'NONE',  ( -1.000000000000000000, 0.000000000000000000, 0.000000000000000000 ) ) ;
#7682=DIRECTION ( 'NONE',  ( 0.000000000000000000, 0.000000000000000000, 1.000000000000000000 ) ) ;
#7711=DIRECTION ( 'NONE',  ( 1.000000000000000000, 0.000000000000000000, 0.000000000000000000 ) ) ;
#7724=DIRECTION ( 'NONE',  ( -1.000000000000000000, 0.000000000000000000, 0.000000000000000000 ) ) ;
#7725=ORIENTED_EDGE ( 'NONE', *, *, #4190, .T. ) ;
#7731=PRODUCT ( 'Cleco, Handle, Rivet', 'Cleco, Handle, Rivet', '', ( #4186 ) ) ;
#7741=EDGE_CURVE ( 'NONE', #1449, #6459, #5718, .T. ) ;
#7744=EDGE_CURVE ( 'NONE', #3669, #1449, #7023, .T. ) ;
#7793=DIRECTION ( 'NONE',  ( -1.000000000000000000, 0.000000000000000000, 0.000000000000000000 ) ) ;
#7795=AXIS2_PLACEMENT_3D ( 'NONE', #7338, #6075, #6728 ) ;
#7804=ORIENTED_EDGE ( 'NONE', *, *, #1291, .T. ) ;
#7806=ORIENTED_EDGE ( 'NONE', *, *, #2742, .F. ) ;
#7812=DIRECTION ( 'NONE',  ( 0.000000000000000000, 0.000000000000000000, 1.000000000000000000 ) ) ;
#7813=DIRECTION ( 'NONE',  ( -1.000000000000000000, 0.000000000000000000, 0.000000000000000000 ) ) ;
#7826=CARTESIAN_POINT ( 'NONE',  ( 0.000000000000000000, 0.000000000000000000, 0.000000000000000000 ) ) ;
#7886=AXIS2_PLACEMENT_3D ( 'NONE', #941, #5812, #4745 ) ;
#7889=CARTESIAN_POINT ( 'NONE',  ( 0.000000000000000000, 0.000000000000000000, -0.6849999999999999423 ) ) ;
#7893=EDGE_LOOP ( 'NONE', ( #3149, #1073, #1094, #7533 ) ) ;
#7895=CIRCLE ( 'NONE', #6472, 0.09374999999999998612 ) ;
#7902=CARTESIAN_POINT ( 'NONE',  ( -0.09374999999999998612, 0.000000000000000000, -0.6849999999999999423 ) ) ;
#7903=CIRCLE ( 'NONE', #3331, 0.1255000000000000282 ) ;
#7925=AXIS2_PLACEMENT_3D ( 'NONE', #3326, #4560, #3206 ) ;
#7935=ADVANCED_FACE ( 'NONE', ( #510 ), #4423, .T. ) ;
#7940=AXIS2_PLACEMENT_3D ( 'NONE', #4762, #4150, #1035 ) ;
#7962=CARTESIAN_POINT ( 'NONE',  ( 0.000000000000000000, 0.000000000000000000, -0.6537499999999999423 ) ) ;
#7970=DIRECTION ( 'NONE',  ( 0.000000000000000000, 0.000000000000000000, -1.000000000000000000 ) ) ;
#7975=EDGE_CURVE ( 'NONE', #255, #646, #3764, .T. ) ;
#7977=FACE_OUTER_BOUND ( 'NONE', #2375, .T. ) ;
#7989=( CONVERSION_BASED_UNIT ( 'INCH', #3007 ) LENGTH_UNIT ( ) NAMED_UNIT ( #4994 ) );
#7993=DIRECTION ( 'NONE',  ( -0.000000000000000000, -0.000000000000000000, -1.000000000000000000 ) ) ;
#8016=CYLINDRICAL_SURFACE ( 'NONE', #192, 0.06250000000000000000 ) ;
#8022=ORIENTED_EDGE ( 'NONE', *, *, #985, .T. ) ;
#8023=FACE_OUTER_BOUND ( 'NONE', #184, .T. ) ;
#8032=AXIS2_PLACEMENT_3D ( 'NONE', #5014, #1699, #6173 ) ;
#8039=DIRECTION ( 'NONE',  ( 0.000000000000000000, 0.000000000000000000, -1.000000000000000000 ) ) ;
#8046=CARTESIAN_POINT ( 'NONE',  ( -0.1255000000000000282, 1.536931732929928570E-17, 0.06300000000000000044 ) ) ;
#8072=EDGE_CURVE ( 'NONE', #2236, #2877, #3910, .T. ) ;
#8076=ORIENTED_EDGE ( 'NONE', *, *, #8072, .T. ) ;
#8081=EDGE_CURVE ( 'NONE', #19, #2657, #5268, .T. ) ;
#8108=COLOUR_RGB('Light Blue', 0.31764706, 0.68627451, 0.89019608);
#8109=FILL_AREA_STYLE_COLOUR('',#8108);
#8110=FILL_AREA_STYLE('',(#8109));
#8111=SURFACE_STYLE_FILL_AREA(#8110);
#8112=SURFACE_SIDE_STYLE('',(#8111));
#8113=SURFACE_STYLE_USAGE(.BOTH.,#8112);
#8114=PRESENTATION_STYLE_ASSIGNMENT((#8113));
#8156=STYLED_ITEM('',(#8114),#3575);
#8157=MECHANICAL_DESIGN_GEOMETRIC_PRESENTATION_REPRESENTATION('',(#8156),#6058);
ENDSEC;
END-ISO-10303-21;
